ISO-10303-21;
HEADER;
/* Generated by software containing ST-Developer
 * from STEP Tools, Inc. (www.steptools.com) 
 */

FILE_DESCRIPTION(
/* description */ ('Five-roller gravity conveyor'),
/* implementation_level */ '2;1');

FILE_NAME(
/* name */ 'Cap Screw - M4x16.step',
/* time_stamp */ '2026-10-29T15:36:43-07:00',
/* author */ (''),
/* organization */ (''),
/* preprocessor_version */ 'ST-DEVELOPER v20.2',
/* originating_system */ 'Autodesk Translation Framework v15.17.0.0',
/* authorisation */ '');

FILE_SCHEMA (('AUTOMOTIVE_DESIGN { 1 0 10303 214 3 1 1 }'));
ENDSEC;

DATA;
#10=MECHANICAL_DESIGN_GEOMETRIC_PRESENTATION_REPRESENTATION('',(#337),#7806);
#268=CONICAL_SURFACE('',#4838,0.325,0.785398163397448);
#269=CONICAL_SURFACE('',#4842,0.335,0.785398163397448);
#270=CONICAL_SURFACE('',#4846,0.21,0.463647609000806);
#271=CONICAL_SURFACE('',#4850,0.18,0.785398163397448);
#273=ORIENTED_CLOSED_SHELL('',*,#4226,.F.);
#275=BREP_WITH_VOIDS('Body1',#4225,(#273));
#293=SHAPE_REPRESENTATION_RELATIONSHIP('SRR','None',#7932,#311);
#311=ADVANCED_BREP_SHAPE_REPRESENTATION('',(#275),#7805);
#337=STYLED_ITEM('',(#8098),#275);
#420=FACE_BOUND('',#1162,.T.);
#586=CIRCLE('',#4837,0.3);
#587=CIRCLE('',#4839,0.35);
#588=CIRCLE('',#4841,0.35);
#589=CIRCLE('',#4843,0.32);
#590=CIRCLE('',#4845,0.22);
#591=CIRCLE('',#4847,0.1954);
#592=CIRCLE('',#4849,0.1954);
#593=CIRCLE('',#4851,0.16);
#650=CYLINDRICAL_SURFACE('',#4840,0.35);
#651=CYLINDRICAL_SURFACE('',#4848,0.1954);
#867=FACE_OUTER_BOUND('',#1157,.T.);
#868=FACE_OUTER_BOUND('',#1158,.T.);
#869=FACE_OUTER_BOUND('',#1159,.T.);
#870=FACE_OUTER_BOUND('',#1160,.T.);
#871=FACE_OUTER_BOUND('',#1161,.T.);
#872=FACE_OUTER_BOUND('',#1163,.T.);
#873=FACE_OUTER_BOUND('',#1164,.T.);
#874=FACE_OUTER_BOUND('',#1165,.T.);
#875=FACE_OUTER_BOUND('',#1166,.T.);
#876=FACE_OUTER_BOUND('',#1167,.T.);
#877=FACE_OUTER_BOUND('',#1168,.T.);
#878=FACE_OUTER_BOUND('',#1169,.T.);
#879=FACE_OUTER_BOUND('',#1170,.T.);
#880=FACE_OUTER_BOUND('',#1171,.T.);
#881=FACE_OUTER_BOUND('',#1172,.T.);
#882=FACE_OUTER_BOUND('',#1173,.T.);
#883=FACE_OUTER_BOUND('',#1174,.T.);
#1157=EDGE_LOOP('',(#3758));
#1158=EDGE_LOOP('',(#3759,#3760,#3761,#3762));
#1159=EDGE_LOOP('',(#3763,#3764,#3765,#3766));
#1160=EDGE_LOOP('',(#3767,#3768,#3769,#3770));
#1161=EDGE_LOOP('',(#3771));
#1162=EDGE_LOOP('',(#3772));
#1163=EDGE_LOOP('',(#3773,#3774,#3775,#3776));
#1164=EDGE_LOOP('',(#3777,#3778,#3779,#3780));
#1165=EDGE_LOOP('',(#3781,#3782,#3783,#3784));
#1166=EDGE_LOOP('',(#3785));
#1167=EDGE_LOOP('',(#3786,#3787,#3788,#3789));
#1168=EDGE_LOOP('',(#3790,#3791,#3792,#3793));
#1169=EDGE_LOOP('',(#3794,#3795,#3796,#3797));
#1170=EDGE_LOOP('',(#3798,#3799,#3800,#3801));
#1171=EDGE_LOOP('',(#3802,#3803,#3804,#3805));
#1172=EDGE_LOOP('',(#3806,#3807,#3808,#3809));
#1173=EDGE_LOOP('',(#3810,#3811,#3812,#3813,#3814,#3815));
#1174=EDGE_LOOP('',(#3816,#3817,#3818,#3819,#3820,#3821));
#1492=LINE('',#7648,#1833);
#1493=LINE('',#7652,#1834);
#1494=LINE('',#7656,#1835);
#1495=LINE('',#7663,#1836);
#1496=LINE('',#7667,#1837);
#1497=LINE('',#7671,#1838);
#1498=LINE('',#7676,#1839);
#1499=LINE('',#7678,#1840);
#1500=LINE('',#7680,#1841);
#1501=LINE('',#7681,#1842);
#1502=LINE('',#7684,#1843);
#1503=LINE('',#7686,#1844);
#1504=LINE('',#7687,#1845);
#1505=LINE('',#7690,#1846);
#1506=LINE('',#7692,#1847);
#1507=LINE('',#7693,#1848);
#1508=LINE('',#7696,#1849);
#1509=LINE('',#7698,#1850);
#1510=LINE('',#7699,#1851);
#1511=LINE('',#7702,#1852);
#1512=LINE('',#7704,#1853);
#1513=LINE('',#7705,#1854);
#1514=LINE('',#7707,#1855);
#1515=LINE('',#7708,#1856);
#1833=VECTOR('',#6054,0.325);
#1834=VECTOR('',#6059,0.35);
#1835=VECTOR('',#6064,0.335);
#1836=VECTOR('',#6073,0.21);
#1837=VECTOR('',#6078,0.2);
#1838=VECTOR('',#6083,0.18);
#1839=VECTOR('',#6088,1.);
#1840=VECTOR('',#6089,1.);
#1841=VECTOR('',#6090,1.);
#1842=VECTOR('',#6091,1.);
#1843=VECTOR('',#6094,1.);
#1844=VECTOR('',#6095,1.);
#1845=VECTOR('',#6096,1.);
#1846=VECTOR('',#6099,1.);
#1847=VECTOR('',#6100,1.);
#1848=VECTOR('',#6101,1.);
#1849=VECTOR('',#6104,1.);
#1850=VECTOR('',#6105,1.);
#1851=VECTOR('',#6106,1.);
#1852=VECTOR('',#6109,1.);
#1853=VECTOR('',#6110,1.);
#1854=VECTOR('',#6111,1.);
#1855=VECTOR('',#6114,1.);
#1856=VECTOR('',#6115,1.);
#2200=VERTEX_POINT('',#7643);
#2201=VERTEX_POINT('',#7646);
#2202=VERTEX_POINT('',#7650);
#2203=VERTEX_POINT('',#7654);
#2204=VERTEX_POINT('',#7658);
#2205=VERTEX_POINT('',#7661);
#2206=VERTEX_POINT('',#7665);
#2207=VERTEX_POINT('',#7669);
#2208=VERTEX_POINT('',#7674);
#2209=VERTEX_POINT('',#7675);
#2210=VERTEX_POINT('',#7677);
#2211=VERTEX_POINT('',#7679);
#2212=VERTEX_POINT('',#7683);
#2213=VERTEX_POINT('',#7685);
#2214=VERTEX_POINT('',#7689);
#2215=VERTEX_POINT('',#7691);
#2216=VERTEX_POINT('',#7695);
#2217=VERTEX_POINT('',#7697);
#2218=VERTEX_POINT('',#7701);
#2219=VERTEX_POINT('',#7703);
#2722=EDGE_CURVE('',#2200,#2200,#586,.T.);
#2723=EDGE_CURVE('',#2201,#2201,#587,.T.);
#2724=EDGE_CURVE('',#2201,#2200,#1492,.T.);
#2725=EDGE_CURVE('',#2202,#2202,#588,.T.);
#2726=EDGE_CURVE('',#2202,#2201,#1493,.T.);
#2727=EDGE_CURVE('',#2203,#2203,#589,.T.);
#2728=EDGE_CURVE('',#2203,#2202,#1494,.T.);
#2729=EDGE_CURVE('',#2204,#2204,#590,.T.);
#2730=EDGE_CURVE('',#2205,#2205,#591,.F.);
#2731=EDGE_CURVE('',#2205,#2204,#1495,.T.);
#2732=EDGE_CURVE('',#2206,#2206,#592,.F.);
#2733=EDGE_CURVE('',#2206,#2205,#1496,.T.);
#2734=EDGE_CURVE('',#2207,#2207,#593,.T.);
#2735=EDGE_CURVE('',#2207,#2206,#1497,.T.);
#2736=EDGE_CURVE('',#2208,#2209,#1498,.T.);
#2737=EDGE_CURVE('',#2209,#2210,#1499,.T.);
#2738=EDGE_CURVE('',#2210,#2211,#1500,.T.);
#2739=EDGE_CURVE('',#2208,#2211,#1501,.T.);
#2740=EDGE_CURVE('',#2209,#2212,#1502,.T.);
#2741=EDGE_CURVE('',#2212,#2213,#1503,.T.);
#2742=EDGE_CURVE('',#2213,#2210,#1504,.T.);
#2743=EDGE_CURVE('',#2212,#2214,#1505,.T.);
#2744=EDGE_CURVE('',#2214,#2215,#1506,.T.);
#2745=EDGE_CURVE('',#2215,#2213,#1507,.T.);
#2746=EDGE_CURVE('',#2214,#2216,#1508,.T.);
#2747=EDGE_CURVE('',#2216,#2217,#1509,.T.);
#2748=EDGE_CURVE('',#2217,#2215,#1510,.T.);
#2749=EDGE_CURVE('',#2216,#2218,#1511,.T.);
#2750=EDGE_CURVE('',#2218,#2219,#1512,.T.);
#2751=EDGE_CURVE('',#2219,#2217,#1513,.T.);
#2752=EDGE_CURVE('',#2218,#2208,#1514,.T.);
#2753=EDGE_CURVE('',#2211,#2219,#1515,.T.);
#3758=ORIENTED_EDGE('',*,*,#2722,.F.);
#3759=ORIENTED_EDGE('',*,*,#2723,.F.);
#3760=ORIENTED_EDGE('',*,*,#2724,.T.);
#3761=ORIENTED_EDGE('',*,*,#2722,.T.);
#3762=ORIENTED_EDGE('',*,*,#2724,.F.);
#3763=ORIENTED_EDGE('',*,*,#2725,.F.);
#3764=ORIENTED_EDGE('',*,*,#2726,.T.);
#3765=ORIENTED_EDGE('',*,*,#2723,.T.);
#3766=ORIENTED_EDGE('',*,*,#2726,.F.);
#3767=ORIENTED_EDGE('',*,*,#2727,.F.);
#3768=ORIENTED_EDGE('',*,*,#2728,.T.);
#3769=ORIENTED_EDGE('',*,*,#2725,.T.);
#3770=ORIENTED_EDGE('',*,*,#2728,.F.);
#3771=ORIENTED_EDGE('',*,*,#2727,.T.);
#3772=ORIENTED_EDGE('',*,*,#2729,.F.);
#3773=ORIENTED_EDGE('',*,*,#2730,.F.);
#3774=ORIENTED_EDGE('',*,*,#2731,.T.);
#3775=ORIENTED_EDGE('',*,*,#2729,.T.);
#3776=ORIENTED_EDGE('',*,*,#2731,.F.);
#3777=ORIENTED_EDGE('',*,*,#2732,.F.);
#3778=ORIENTED_EDGE('',*,*,#2733,.T.);
#3779=ORIENTED_EDGE('',*,*,#2730,.T.);
#3780=ORIENTED_EDGE('',*,*,#2733,.F.);
#3781=ORIENTED_EDGE('',*,*,#2734,.F.);
#3782=ORIENTED_EDGE('',*,*,#2735,.T.);
#3783=ORIENTED_EDGE('',*,*,#2732,.T.);
#3784=ORIENTED_EDGE('',*,*,#2735,.F.);
#3785=ORIENTED_EDGE('',*,*,#2734,.T.);
#3786=ORIENTED_EDGE('',*,*,#2736,.T.);
#3787=ORIENTED_EDGE('',*,*,#2737,.T.);
#3788=ORIENTED_EDGE('',*,*,#2738,.T.);
#3789=ORIENTED_EDGE('',*,*,#2739,.F.);
#3790=ORIENTED_EDGE('',*,*,#2740,.T.);
#3791=ORIENTED_EDGE('',*,*,#2741,.T.);
#3792=ORIENTED_EDGE('',*,*,#2742,.T.);
#3793=ORIENTED_EDGE('',*,*,#2737,.F.);
#3794=ORIENTED_EDGE('',*,*,#2743,.T.);
#3795=ORIENTED_EDGE('',*,*,#2744,.T.);
#3796=ORIENTED_EDGE('',*,*,#2745,.T.);
#3797=ORIENTED_EDGE('',*,*,#2741,.F.);
#3798=ORIENTED_EDGE('',*,*,#2746,.T.);
#3799=ORIENTED_EDGE('',*,*,#2747,.T.);
#3800=ORIENTED_EDGE('',*,*,#2748,.T.);
#3801=ORIENTED_EDGE('',*,*,#2744,.F.);
#3802=ORIENTED_EDGE('',*,*,#2749,.T.);
#3803=ORIENTED_EDGE('',*,*,#2750,.T.);
#3804=ORIENTED_EDGE('',*,*,#2751,.T.);
#3805=ORIENTED_EDGE('',*,*,#2747,.F.);
#3806=ORIENTED_EDGE('',*,*,#2752,.T.);
#3807=ORIENTED_EDGE('',*,*,#2739,.T.);
#3808=ORIENTED_EDGE('',*,*,#2753,.T.);
#3809=ORIENTED_EDGE('',*,*,#2750,.F.);
#3810=ORIENTED_EDGE('',*,*,#2752,.F.);
#3811=ORIENTED_EDGE('',*,*,#2749,.F.);
#3812=ORIENTED_EDGE('',*,*,#2746,.F.);
#3813=ORIENTED_EDGE('',*,*,#2743,.F.);
#3814=ORIENTED_EDGE('',*,*,#2740,.F.);
#3815=ORIENTED_EDGE('',*,*,#2736,.F.);
#3816=ORIENTED_EDGE('',*,*,#2753,.F.);
#3817=ORIENTED_EDGE('',*,*,#2738,.F.);
#3818=ORIENTED_EDGE('',*,*,#2742,.F.);
#3819=ORIENTED_EDGE('',*,*,#2745,.F.);
#3820=ORIENTED_EDGE('',*,*,#2748,.F.);
#3821=ORIENTED_EDGE('',*,*,#2751,.F.);
#3956=PLANE('',#4836);
#3957=PLANE('',#4844);
#3958=PLANE('',#4852);
#3959=PLANE('',#4853);
#3960=PLANE('',#4854);
#3961=PLANE('',#4855);
#3962=PLANE('',#4856);
#3963=PLANE('',#4857);
#3964=PLANE('',#4858);
#3965=PLANE('',#4859);
#3966=PLANE('',#4860);
#4182=ADVANCED_FACE('',(#867),#3956,.T.);
#4183=ADVANCED_FACE('',(#868),#268,.T.);
#4184=ADVANCED_FACE('',(#869),#650,.T.);
#4185=ADVANCED_FACE('',(#870),#269,.T.);
#4186=ADVANCED_FACE('',(#871,#420),#3957,.T.);
#4187=ADVANCED_FACE('',(#872),#270,.T.);
#4188=ADVANCED_FACE('',(#873),#651,.T.);
#4189=ADVANCED_FACE('',(#874),#271,.T.);
#4190=ADVANCED_FACE('',(#875),#3958,.T.);
#4191=ADVANCED_FACE('',(#876),#3959,.F.);
#4192=ADVANCED_FACE('',(#877),#3960,.F.);
#4193=ADVANCED_FACE('',(#878),#3961,.F.);
#4194=ADVANCED_FACE('',(#879),#3962,.F.);
#4195=ADVANCED_FACE('',(#880),#3963,.F.);
#4196=ADVANCED_FACE('',(#881),#3964,.F.);
#4197=ADVANCED_FACE('',(#882),#3965,.F.);
#4198=ADVANCED_FACE('',(#883),#3966,.F.);
#4225=CLOSED_SHELL('',(#4182,#4183,#4184,#4185,#4186,#4187,#4188,#4189,
#4190));
#4226=CLOSED_SHELL('',(#4191,#4192,#4193,#4194,#4195,#4196,#4197,#4198));
#4835=AXIS2_PLACEMENT_3D('',#7641,#6044,#6045);
#4836=AXIS2_PLACEMENT_3D('',#7642,#6046,#6047);
#4837=AXIS2_PLACEMENT_3D('',#7644,#6048,#6049);
#4838=AXIS2_PLACEMENT_3D('',#7645,#6050,#6051);
#4839=AXIS2_PLACEMENT_3D('',#7647,#6052,#6053);
#4840=AXIS2_PLACEMENT_3D('',#7649,#6055,#6056);
#4841=AXIS2_PLACEMENT_3D('',#7651,#6057,#6058);
#4842=AXIS2_PLACEMENT_3D('',#7653,#6060,#6061);
#4843=AXIS2_PLACEMENT_3D('',#7655,#6062,#6063);
#4844=AXIS2_PLACEMENT_3D('',#7657,#6065,#6066);
#4845=AXIS2_PLACEMENT_3D('',#7659,#6067,#6068);
#4846=AXIS2_PLACEMENT_3D('',#7660,#6069,#6070);
#4847=AXIS2_PLACEMENT_3D('',#7662,#6071,#6072);
#4848=AXIS2_PLACEMENT_3D('',#7664,#6074,#6075);
#4849=AXIS2_PLACEMENT_3D('',#7666,#6076,#6077);
#4850=AXIS2_PLACEMENT_3D('',#7668,#6079,#6080);
#4851=AXIS2_PLACEMENT_3D('',#7670,#6081,#6082);
#4852=AXIS2_PLACEMENT_3D('',#7672,#6084,#6085);
#4853=AXIS2_PLACEMENT_3D('',#7673,#6086,#6087);
#4854=AXIS2_PLACEMENT_3D('',#7682,#6092,#6093);
#4855=AXIS2_PLACEMENT_3D('',#7688,#6097,#6098);
#4856=AXIS2_PLACEMENT_3D('',#7694,#6102,#6103);
#4857=AXIS2_PLACEMENT_3D('',#7700,#6107,#6108);
#4858=AXIS2_PLACEMENT_3D('',#7706,#6112,#6113);
#4859=AXIS2_PLACEMENT_3D('',#7709,#6116,#6117);
#4860=AXIS2_PLACEMENT_3D('',#7710,#6118,#6119);
#6044=DIRECTION('axis',(0.,0.,1.));
#6045=DIRECTION('refdir',(1.,0.,0.));
#6046=DIRECTION('center_axis',(0.,1.,0.));
#6047=DIRECTION('ref_axis',(0.,0.,1.));
#6048=DIRECTION('center_axis',(0.,-1.,0.));
#6049=DIRECTION('ref_axis',(1.,0.,0.));
#6050=DIRECTION('center_axis',(0.,-1.,0.));
#6051=DIRECTION('ref_axis',(1.,0.,0.));
#6052=DIRECTION('center_axis',(0.,-1.,0.));
#6053=DIRECTION('ref_axis',(1.,0.,0.));
#6054=DIRECTION('',(0.707106781186547,0.707106781186548,8.65956056235493E-17));
#6055=DIRECTION('center_axis',(0.,-1.,0.));
#6056=DIRECTION('ref_axis',(1.,0.,0.));
#6057=DIRECTION('center_axis',(0.,-1.,0.));
#6058=DIRECTION('ref_axis',(1.,0.,0.));
#6059=DIRECTION('',(0.,1.,0.));
#6060=DIRECTION('center_axis',(0.,1.,0.));
#6061=DIRECTION('ref_axis',(1.,0.,0.));
#6062=DIRECTION('center_axis',(0.,-1.,0.));
#6063=DIRECTION('ref_axis',(1.,0.,0.));
#6064=DIRECTION('',(-0.707106781186547,0.707106781186548,-8.65956056235493E-17));
#6065=DIRECTION('center_axis',(0.,-1.,0.));
#6066=DIRECTION('ref_axis',(0.,0.,-1.));
#6067=DIRECTION('center_axis',(0.,-1.,0.));
#6068=DIRECTION('ref_axis',(1.,0.,0.));
#6069=DIRECTION('center_axis',(0.,1.,0.));
#6070=DIRECTION('ref_axis',(1.,0.,0.));
#6071=DIRECTION('center_axis',(0.,1.,0.));
#6072=DIRECTION('ref_axis',(1.,0.,0.));
#6073=DIRECTION('',(-0.447213595499958,0.894427190999916,-5.47678698264203E-17));
#6074=DIRECTION('center_axis',(0.,-1.,0.));
#6075=DIRECTION('ref_axis',(1.,0.,0.));
#6076=DIRECTION('center_axis',(0.,1.,0.));
#6077=DIRECTION('ref_axis',(1.,0.,0.));
#6078=DIRECTION('',(0.,1.,0.));
#6079=DIRECTION('center_axis',(0.,1.,0.));
#6080=DIRECTION('ref_axis',(1.,0.,0.));
#6081=DIRECTION('center_axis',(0.,-1.,0.));
#6082=DIRECTION('ref_axis',(1.,0.,0.));
#6083=DIRECTION('',(-0.707106781186547,0.707106781186548,-8.65956056235493E-17));
#6084=DIRECTION('center_axis',(0.,-1.,0.));
#6085=DIRECTION('ref_axis',(0.,0.,-1.));
#6086=DIRECTION('center_axis',(0.866025403784439,0.,-0.5));
#6087=DIRECTION('ref_axis',(0.5,0.,0.866025403784439));
#6088=DIRECTION('',(-0.5,0.,-0.866025403784439));
#6089=DIRECTION('',(0.,-1.,0.));
#6090=DIRECTION('',(0.5,0.,0.866025403784439));
#6091=DIRECTION('',(0.,-1.,0.));
#6092=DIRECTION('center_axis',(1.60246890531964E-16,0.,-1.));
#6093=DIRECTION('ref_axis',(1.,0.,1.60246890531964E-16));
#6094=DIRECTION('',(-1.,0.,-1.60246890531964E-16));
#6095=DIRECTION('',(0.,-1.,0.));
#6096=DIRECTION('',(1.,0.,1.60246890531964E-16));
#6097=DIRECTION('center_axis',(-0.866025403784439,0.,-0.5));
#6098=DIRECTION('ref_axis',(0.5,0.,-0.866025403784439));
#6099=DIRECTION('',(-0.5,0.,0.866025403784439));
#6100=DIRECTION('',(0.,-1.,0.));
#6101=DIRECTION('',(0.5,0.,-0.866025403784439));
#6102=DIRECTION('center_axis',(-0.866025403784439,0.,0.5));
#6103=DIRECTION('ref_axis',(-0.5,0.,-0.866025403784439));
#6104=DIRECTION('',(0.5,0.,0.866025403784439));
#6105=DIRECTION('',(0.,-1.,0.));
#6106=DIRECTION('',(-0.5,0.,-0.866025403784439));
#6107=DIRECTION('center_axis',(-1.60246890531964E-16,0.,1.));
#6108=DIRECTION('ref_axis',(-1.,0.,-1.60246890531964E-16));
#6109=DIRECTION('',(1.,0.,1.60246890531964E-16));
#6110=DIRECTION('',(0.,-1.,0.));
#6111=DIRECTION('',(-1.,0.,-1.60246890531964E-16));
#6112=DIRECTION('center_axis',(0.866025403784439,0.,0.5));
#6113=DIRECTION('ref_axis',(-0.5,0.,0.866025403784439));
#6114=DIRECTION('',(0.5,0.,-0.866025403784439));
#6115=DIRECTION('',(-0.5,0.,0.866025403784439));
#6116=DIRECTION('center_axis',(0.,1.,0.));
#6117=DIRECTION('ref_axis',(1.,0.,0.));
#6118=DIRECTION('center_axis',(0.,-1.,0.));
#6119=DIRECTION('ref_axis',(0.,0.,-1.));
#7641=CARTESIAN_POINT('',(0.,0.,0.));
#7642=CARTESIAN_POINT('Origin',(0.3,0.4,0.));
#7643=CARTESIAN_POINT('',(-0.3,0.4,-3.67394039744206E-17));
#7644=CARTESIAN_POINT('Origin',(0.,0.4,0.));
#7645=CARTESIAN_POINT('Origin',(0.,0.375,0.));
#7646=CARTESIAN_POINT('',(-0.35,0.35,-4.28626379701573E-17));
#7647=CARTESIAN_POINT('Origin',(0.,0.35,0.));
#7648=CARTESIAN_POINT('',(-0.325,0.375,-3.9801020972289E-17));
#7649=CARTESIAN_POINT('Origin',(0.,0.19,0.));
#7650=CARTESIAN_POINT('',(-0.35,0.03,-4.28626379701574E-17));
#7651=CARTESIAN_POINT('Origin',(0.,0.03,0.));
#7652=CARTESIAN_POINT('',(-0.35,0.19,-4.28626379701574E-17));
#7653=CARTESIAN_POINT('Origin',(0.,0.0149999999999999,0.));
#7654=CARTESIAN_POINT('',(-0.32,-3.29597460435593E-17,-3.91886975727153E-17));
#7655=CARTESIAN_POINT('Origin',(0.,0.,0.));
#7656=CARTESIAN_POINT('',(-0.335,0.0149999999999999,-4.10256677714363E-17));
#7657=CARTESIAN_POINT('Origin',(0.22,0.,0.));
#7658=CARTESIAN_POINT('',(-0.22,-6.93889390390723E-18,-2.69422295812418E-17));
#7659=CARTESIAN_POINT('Origin',(0.,0.,0.));
#7660=CARTESIAN_POINT('Origin',(0.,-0.02,0.));
#7661=CARTESIAN_POINT('',(-0.1954,-0.0492,2.39295984553393E-17));
#7662=CARTESIAN_POINT('Origin',(0.,-0.0492,0.));
#7663=CARTESIAN_POINT('',(-0.21,-0.02,-2.57175827820944E-17));
#7664=CARTESIAN_POINT('Origin',(0.,-0.8,0.));
#7665=CARTESIAN_POINT('',(-0.1954,-1.5646,2.39295984553393E-17));
#7666=CARTESIAN_POINT('Origin',(0.,-1.5646,0.));
#7667=CARTESIAN_POINT('',(-0.1954,-0.8,-2.39295984553393E-17));
#7668=CARTESIAN_POINT('Origin',(0.,-1.58,0.));
#7669=CARTESIAN_POINT('',(-0.16,-1.6,-1.95943487863577E-17));
#7670=CARTESIAN_POINT('Origin',(0.,-1.6,0.));
#7671=CARTESIAN_POINT('',(-0.18,-1.58,-2.20436423846524E-17));
#7672=CARTESIAN_POINT('Origin',(0.,-1.6,0.));
#7673=CARTESIAN_POINT('Origin',(0.0866025403784439,-0.4,-0.15));
#7674=CARTESIAN_POINT('',(0.173205080756888,-0.4,0.));
#7675=CARTESIAN_POINT('',(0.0866025403784439,-0.4,-0.15));
#7676=CARTESIAN_POINT('',(0.173205080756888,-0.4,0.));
#7677=CARTESIAN_POINT('',(0.0866025403784439,-0.64,-0.15));
#7678=CARTESIAN_POINT('',(0.0866025403784439,-0.4,-0.15));
#7679=CARTESIAN_POINT('',(0.173205080756888,-0.64,0.));
#7680=CARTESIAN_POINT('',(0.173205080756888,-0.64,0.));
#7681=CARTESIAN_POINT('',(0.173205080756888,-0.4,0.));
#7682=CARTESIAN_POINT('Origin',(-0.0866025403784438,-0.4,-0.15));
#7683=CARTESIAN_POINT('',(-0.0866025403784438,-0.4,-0.15));
#7684=CARTESIAN_POINT('',(0.0866025403784439,-0.4,-0.15));
#7685=CARTESIAN_POINT('',(-0.0866025403784438,-0.64,-0.15));
#7686=CARTESIAN_POINT('',(-0.0866025403784438,-0.4,-0.15));
#7687=CARTESIAN_POINT('',(0.0866025403784439,-0.64,-0.15));
#7688=CARTESIAN_POINT('Origin',(-0.173205080756888,-0.4,-2.77555756156289E-17));
#7689=CARTESIAN_POINT('',(-0.173205080756888,-0.4,-2.12115047744981E-17));
#7690=CARTESIAN_POINT('',(-0.0866025403784438,-0.4,-0.15));
#7691=CARTESIAN_POINT('',(-0.173205080756888,-0.64,-2.77555756156289E-17));
#7692=CARTESIAN_POINT('',(-0.173205080756888,-0.4,-2.12115047744981E-17));
#7693=CARTESIAN_POINT('',(-0.0866025403784438,-0.64,-0.15));
#7694=CARTESIAN_POINT('Origin',(-0.0866025403784439,-0.4,0.15));
#7695=CARTESIAN_POINT('',(-0.0866025403784439,-0.4,0.15));
#7696=CARTESIAN_POINT('',(-0.173205080756888,-0.4,-2.12115047744981E-17));
#7697=CARTESIAN_POINT('',(-0.0866025403784439,-0.64,0.15));
#7698=CARTESIAN_POINT('',(-0.0866025403784439,-0.4,0.15));
#7699=CARTESIAN_POINT('',(-0.173205080756888,-0.64,-2.12115047744981E-17));
#7700=CARTESIAN_POINT('Origin',(0.0866025403784439,-0.4,0.15));
#7701=CARTESIAN_POINT('',(0.0866025403784439,-0.4,0.15));
#7702=CARTESIAN_POINT('',(-0.0866025403784439,-0.4,0.15));
#7703=CARTESIAN_POINT('',(0.0866025403784439,-0.64,0.15));
#7704=CARTESIAN_POINT('',(0.0866025403784439,-0.4,0.15));
#7705=CARTESIAN_POINT('',(-0.0866025403784439,-0.64,0.15));
#7706=CARTESIAN_POINT('Origin',(0.173205080756888,-0.4,0.));
#7707=CARTESIAN_POINT('',(0.0866025403784439,-0.4,0.15));
#7708=CARTESIAN_POINT('',(0.0866025403784439,-0.64,0.15));
#7709=CARTESIAN_POINT('Origin',(0.,-0.4,-2.77555756156289E-17));
#7710=CARTESIAN_POINT('Origin',(0.,-0.64,-2.77555756156289E-17));
#7781=UNCERTAINTY_MEASURE_WITH_UNIT(LENGTH_MEASURE(0.001),#7807,
'DISTANCE_ACCURACY_VALUE',
'Maximum model space distance between geometric entities at asserted c
onnectivities');
#7782=UNCERTAINTY_MEASURE_WITH_UNIT(LENGTH_MEASURE(0.001),#7807,
'DISTANCE_ACCURACY_VALUE',
'Maximum model space distance between geometric entities at asserted c
onnectivities');
#7805=(
GEOMETRIC_REPRESENTATION_CONTEXT(3)
GLOBAL_UNCERTAINTY_ASSIGNED_CONTEXT((#7781))
GLOBAL_UNIT_ASSIGNED_CONTEXT((#7807,#7809,#7810))
REPRESENTATION_CONTEXT('','3D')
);
#7806=(
GEOMETRIC_REPRESENTATION_CONTEXT(3)
GLOBAL_UNCERTAINTY_ASSIGNED_CONTEXT((#7782))
GLOBAL_UNIT_ASSIGNED_CONTEXT((#7807,#7809,#7810))
REPRESENTATION_CONTEXT('','3D')
);
#7807=(
LENGTH_UNIT()
NAMED_UNIT(*)
SI_UNIT(.CENTI.,.METRE.)
);
#7809=(
NAMED_UNIT(*)
PLANE_ANGLE_UNIT()
SI_UNIT($,.RADIAN.)
);
#7810=(
NAMED_UNIT(*)
SI_UNIT($,.STERADIAN.)
SOLID_ANGLE_UNIT()
);
#7833=SHAPE_DEFINITION_REPRESENTATION(#7861,#7932);
#7861=PRODUCT_DEFINITION_SHAPE('',$,#7956);
#7932=SHAPE_REPRESENTATION('',(#4835),#7805);
#7933=PRODUCT_DEFINITION_CONTEXT('part definition',#8004,'design');
#7956=PRODUCT_DEFINITION('Cap Screw - M4x16','Cap Screw - M4x16',#7979,
#7933);
#7979=PRODUCT_DEFINITION_FORMATION('',$,#8028);
#8004=APPLICATION_CONTEXT(
'Core Data for Automotive Mechanical Design Process');
#8005=PRODUCT_CONTEXT('part definition',#8004,'mechanical');
#8028=PRODUCT('Cap Screw - M4x16','Cap Screw - M4x16',
'Cap Screw - M4x16',(#8005));
#8092=COLOUR_RGB('Black',0.12,0.14,0.17);
#8093=FILL_AREA_STYLE_COLOUR('',#8092);
#8094=FILL_AREA_STYLE('',(#8093));
#8095=SURFACE_STYLE_FILL_AREA(#8094);
#8096=SURFACE_SIDE_STYLE('',(#8095));
#8097=SURFACE_STYLE_USAGE(.BOTH.,#8096);
#8098=PRESENTATION_STYLE_ASSIGNMENT((#8097));
ENDSEC;
END-ISO-10303-21;
